ISO-10303-21;
HEADER;
/* Generated by software containing ST-Developer
 * from STEP Tools, Inc. (www.steptools.com) 
 */

FILE_DESCRIPTION(
/* description */ ('PAT-091'),
/* implementation_level */ '2;1');

FILE_NAME(
/* name */ 'Guide shaft (1).step',
/* time_stamp */ '2026-10-27T15:34:44-07:00',
/* author */ (''),
/* organization */ (''),
/* preprocessor_version */ 'ST-DEVELOPER v20.2',
/* originating_system */ 'Autodesk Translation Framework v15.17.0.0',
/* authorisation */ '');

FILE_SCHEMA (('AUTOMOTIVE_DESIGN { 1 0 10303 214 3 1 1 }'));
ENDSEC;

DATA;
#10=MECHANICAL_DESIGN_GEOMETRIC_PRESENTATION_REPRESENTATION('',(#981),#25100);
#761=SHAPE_REPRESENTATION_RELATIONSHIP('SRR','None',#25522,#871);
#871=ADVANCED_BREP_SHAPE_REPRESENTATION('',(#1105),#24992);
#981=STYLED_ITEM('',(#26191),#1105);
#1105=MANIFOLD_SOLID_BREP('Body1',#13258);
#1692=PLANE('',#14833);
#1693=PLANE('',#14834);
#2175=FACE_OUTER_BOUND('',#3099,.T.);
#2176=FACE_OUTER_BOUND('',#3100,.T.);
#2177=FACE_OUTER_BOUND('',#3101,.T.);
#3099=EDGE_LOOP('',(#9500,#9501,#9502,#9503));
#3100=EDGE_LOOP('',(#9504));
#3101=EDGE_LOOP('',(#9505));
#4268=LINE('',#21543,#5008);
#5008=VECTOR('',#17106,0.6);
#5724=CIRCLE('',#14831,0.6);
#5725=CIRCLE('',#14832,0.6);
#6559=VERTEX_POINT('',#21540);
#6560=VERTEX_POINT('',#21542);
#7685=EDGE_CURVE('',#6559,#6559,#5724,.T.);
#7686=EDGE_CURVE('',#6559,#6560,#4268,.T.);
#7687=EDGE_CURVE('',#6560,#6560,#5725,.T.);
#9500=ORIENTED_EDGE('',*,*,#7685,.F.);
#9501=ORIENTED_EDGE('',*,*,#7686,.T.);
#9502=ORIENTED_EDGE('',*,*,#7687,.T.);
#9503=ORIENTED_EDGE('',*,*,#7686,.F.);
#9504=ORIENTED_EDGE('',*,*,#7685,.T.);
#9505=ORIENTED_EDGE('',*,*,#7687,.F.);
#12134=CYLINDRICAL_SURFACE('',#14830,0.6);
#12542=ADVANCED_FACE('',(#2175),#12134,.T.);
#12543=ADVANCED_FACE('',(#2176),#1692,.T.);
#12544=ADVANCED_FACE('',(#2177),#1693,.F.);
#13258=CLOSED_SHELL('',(#12542,#12543,#12544));
#14829=AXIS2_PLACEMENT_3D('',#21538,#17100,#17101);
#14830=AXIS2_PLACEMENT_3D('',#21539,#17102,#17103);
#14831=AXIS2_PLACEMENT_3D('',#21541,#17104,#17105);
#14832=AXIS2_PLACEMENT_3D('',#21544,#17107,#17108);
#14833=AXIS2_PLACEMENT_3D('',#21545,#17109,#17110);
#14834=AXIS2_PLACEMENT_3D('',#21546,#17111,#17112);
#17100=DIRECTION('axis',(0.,0.,1.));
#17101=DIRECTION('refdir',(1.,0.,0.));
#17102=DIRECTION('center_axis',(1.,0.,0.));
#17103=DIRECTION('ref_axis',(0.,0.,-1.));
#17104=DIRECTION('center_axis',(1.,0.,0.));
#17105=DIRECTION('ref_axis',(0.,0.,-1.));
#17106=DIRECTION('',(-1.,0.,0.));
#17107=DIRECTION('center_axis',(1.,0.,0.));
#17108=DIRECTION('ref_axis',(0.,0.,-1.));
#17109=DIRECTION('center_axis',(1.,0.,0.));
#17110=DIRECTION('ref_axis',(0.,0.,-1.));
#17111=DIRECTION('center_axis',(1.,0.,0.));
#17112=DIRECTION('ref_axis',(0.,0.,-1.));
#21538=CARTESIAN_POINT('',(0.,0.,0.));
#21539=CARTESIAN_POINT('Origin',(-1.,3.,6.));
#21540=CARTESIAN_POINT('',(47.,3.,6.6));
#21541=CARTESIAN_POINT('Origin',(47.,3.,6.));
#21542=CARTESIAN_POINT('',(-1.,3.,6.6));
#21543=CARTESIAN_POINT('',(-1.,3.,6.6));
#21544=CARTESIAN_POINT('Origin',(-1.,3.,6.));
#21545=CARTESIAN_POINT('Origin',(47.,3.,6.));
#21546=CARTESIAN_POINT('Origin',(-1.,3.,6.));
#24871=UNCERTAINTY_MEASURE_WITH_UNIT(LENGTH_MEASURE(0.001),#25101,
'DISTANCE_ACCURACY_VALUE',
'Maximum model space distance between geometric entities at asserted c
onnectivities');
#24979=UNCERTAINTY_MEASURE_WITH_UNIT(LENGTH_MEASURE(0.001),#25101,
'DISTANCE_ACCURACY_VALUE',
'Maximum model space distance between geometric entities at asserted c
onnectivities');
#24992=(
GEOMETRIC_REPRESENTATION_CONTEXT(3)
GLOBAL_UNCERTAINTY_ASSIGNED_CONTEXT((#24871))
GLOBAL_UNIT_ASSIGNED_CONTEXT((#25101,#25103,#25104))
REPRESENTATION_CONTEXT('','3D')
);
#25100=(
GEOMETRIC_REPRESENTATION_CONTEXT(3)
GLOBAL_UNCERTAINTY_ASSIGNED_CONTEXT((#24979))
GLOBAL_UNIT_ASSIGNED_CONTEXT((#25101,#25103,#25104))
REPRESENTATION_CONTEXT('','3D')
);
#25101=(
LENGTH_UNIT()
NAMED_UNIT(*)
SI_UNIT(.CENTI.,.METRE.)
);
#25103=(
NAMED_UNIT(*)
PLANE_ANGLE_UNIT()
SI_UNIT($,.RADIAN.)
);
#25104=(
NAMED_UNIT(*)
SI_UNIT($,.STERADIAN.)
SOLID_ANGLE_UNIT()
);
#25117=SHAPE_DEFINITION_REPRESENTATION(#25237,#25522);
#25237=PRODUCT_DEFINITION_SHAPE('',$,#25643);
#25522=SHAPE_REPRESENTATION('',(#14829),#24992);
#25630=PRODUCT_DEFINITION_CONTEXT('part definition',#25992,'design');
#25643=PRODUCT_DEFINITION('Guide shaft (1)','Guide shaft (1)',#25763,#25630);
#25763=PRODUCT_DEFINITION_FORMATION('',$,#26006);
#25992=APPLICATION_CONTEXT(
'Core Data for Automotive Mechanical Design Process');
#25993=PRODUCT_CONTEXT('part definition',#25992,'mechanical');
#26006=PRODUCT('Guide shaft (1)','Guide shaft (1)','Guide shaft (1)',(#25993));
#26185=COLOUR_RGB('Grey',0.48,0.52,0.57);
#26186=FILL_AREA_STYLE_COLOUR('',#26185);
#26187=FILL_AREA_STYLE('',(#26186));
#26188=SURFACE_STYLE_FILL_AREA(#26187);
#26189=SURFACE_SIDE_STYLE('',(#26188));
#26190=SURFACE_STYLE_USAGE(.BOTH.,#26189);
#26191=PRESENTATION_STYLE_ASSIGNMENT((#26190));
ENDSEC;
END-ISO-10303-21;
